ISO-10303-21;
HEADER;
/* Generated by software containing ST-Developer
 * from STEP Tools, Inc. (www.steptools.com) 
 */

FILE_DESCRIPTION(
/* description */ (''),
/* implementation_level */ '2;1');

FILE_NAME(
/* name */ '10_ISO_8734_Dowel_6x20.step',
/* time_stamp */ '2026-10-11T08:27:52-07:00',
/* author */ (''),
/* organization */ (''),
/* preprocessor_version */ 'ST-DEVELOPER v20.2',
/* originating_system */ 'Autodesk Translation Framework v15.15.0.0',
/* authorisation */ '');

FILE_SCHEMA (('AUTOMOTIVE_DESIGN { 1 0 10303 214 3 1 1 }'));
ENDSEC;

DATA;
#10=MECHANICAL_DESIGN_GEOMETRIC_PRESENTATION_REPRESENTATION('',(#928),#94301);
#900=SHAPE_REPRESENTATION_RELATIONSHIP('SRR','None',#94380,#914);
#914=ADVANCED_BREP_SHAPE_REPRESENTATION('',(#942),#94296);
#928=STYLED_ITEM('',(#94595),#942);
#942=MANIFOLD_SOLID_BREP('Body1',#51027);
#957=TOROIDAL_SURFACE('',#55179,2.06862915010152,0.8);
#1232=CYLINDRICAL_SURFACE('',#55191,3.);
#6602=LINE('',#90618,#11130);
#6603=LINE('',#90627,#11131);
#6604=LINE('',#90629,#11132);
#11130=VECTOR('',#67806,2.7);
#11131=VECTOR('',#67819,2.7);
#11132=VECTOR('',#67822,3.);
#13221=PLANE('',#55186);
#13222=PLANE('',#55187);
#15827=FACE_OUTER_BOUND('',#18588,.T.);
#15828=FACE_OUTER_BOUND('',#18589,.T.);
#15829=FACE_OUTER_BOUND('',#18590,.T.);
#15830=FACE_OUTER_BOUND('',#18591,.T.);
#15831=FACE_OUTER_BOUND('',#18592,.T.);
#15832=FACE_OUTER_BOUND('',#18593,.T.);
#18588=EDGE_LOOP('',(#47593,#47594,#47595,#47596,#47597));
#18589=EDGE_LOOP('',(#47598,#47599,#47600,#47601,#47602));
#18590=EDGE_LOOP('',(#47603));
#18591=EDGE_LOOP('',(#47604));
#18592=EDGE_LOOP('',(#47605,#47606,#47607,#47608));
#18593=EDGE_LOOP('',(#47609,#47610,#47611,#47612));
#20279=CIRCLE('',#55180,2.06862915010152);
#20280=CIRCLE('',#55181,0.8);
#20281=CIRCLE('',#55182,2.63431457505076);
#20282=CIRCLE('',#55183,2.63431457505076);
#20283=CIRCLE('',#55185,3.);
#20284=CIRCLE('',#55188,2.4);
#20285=CIRCLE('',#55190,3.);
#25152=VERTEX_POINT('',#90609);
#25153=VERTEX_POINT('',#90611);
#25154=VERTEX_POINT('',#90613);
#25155=VERTEX_POINT('',#90617);
#25156=VERTEX_POINT('',#90622);
#25157=VERTEX_POINT('',#90625);
#32658=EDGE_CURVE('',#25152,#25152,#20279,.T.);
#32659=EDGE_CURVE('',#25152,#25153,#20280,.T.);
#32660=EDGE_CURVE('',#25153,#25154,#20281,.T.);
#32661=EDGE_CURVE('',#25154,#25153,#20282,.T.);
#32662=EDGE_CURVE('',#25154,#25155,#6602,.T.);
#32663=EDGE_CURVE('',#25155,#25155,#20283,.T.);
#32664=EDGE_CURVE('',#25156,#25156,#20284,.T.);
#32665=EDGE_CURVE('',#25157,#25157,#20285,.T.);
#32666=EDGE_CURVE('',#25157,#25156,#6603,.T.);
#32667=EDGE_CURVE('',#25155,#25157,#6604,.T.);
#47593=ORIENTED_EDGE('',*,*,#32658,.T.);
#47594=ORIENTED_EDGE('',*,*,#32659,.T.);
#47595=ORIENTED_EDGE('',*,*,#32660,.T.);
#47596=ORIENTED_EDGE('',*,*,#32661,.T.);
#47597=ORIENTED_EDGE('',*,*,#32659,.F.);
#47598=ORIENTED_EDGE('',*,*,#32661,.F.);
#47599=ORIENTED_EDGE('',*,*,#32662,.T.);
#47600=ORIENTED_EDGE('',*,*,#32663,.T.);
#47601=ORIENTED_EDGE('',*,*,#32662,.F.);
#47602=ORIENTED_EDGE('',*,*,#32660,.F.);
#47603=ORIENTED_EDGE('',*,*,#32658,.F.);
#47604=ORIENTED_EDGE('',*,*,#32664,.F.);
#47605=ORIENTED_EDGE('',*,*,#32665,.F.);
#47606=ORIENTED_EDGE('',*,*,#32666,.T.);
#47607=ORIENTED_EDGE('',*,*,#32664,.T.);
#47608=ORIENTED_EDGE('',*,*,#32666,.F.);
#47609=ORIENTED_EDGE('',*,*,#32663,.F.);
#47610=ORIENTED_EDGE('',*,*,#32667,.T.);
#47611=ORIENTED_EDGE('',*,*,#32665,.T.);
#47612=ORIENTED_EDGE('',*,*,#32667,.F.);
#48320=CONICAL_SURFACE('',#55184,2.7,0.785398163397448);
#48321=CONICAL_SURFACE('',#55189,2.7,0.785398163397448);
#50914=ADVANCED_FACE('',(#15827),#957,.T.);
#50915=ADVANCED_FACE('',(#15828),#48320,.T.);
#50916=ADVANCED_FACE('',(#15829),#13221,.T.);
#50917=ADVANCED_FACE('',(#15830),#13222,.T.);
#50918=ADVANCED_FACE('',(#15831),#48321,.T.);
#50919=ADVANCED_FACE('',(#15832),#1232,.T.);
#51027=CLOSED_SHELL('',(#50914,#50915,#50916,#50917,#50918,#50919));
#55178=AXIS2_PLACEMENT_3D('',#90607,#67792,#67793);
#55179=AXIS2_PLACEMENT_3D('',#90608,#67794,#67795);
#55180=AXIS2_PLACEMENT_3D('',#90610,#67796,#67797);
#55181=AXIS2_PLACEMENT_3D('',#90612,#67798,#67799);
#55182=AXIS2_PLACEMENT_3D('',#90614,#67800,#67801);
#55183=AXIS2_PLACEMENT_3D('',#90615,#67802,#67803);
#55184=AXIS2_PLACEMENT_3D('',#90616,#67804,#67805);
#55185=AXIS2_PLACEMENT_3D('',#90619,#67807,#67808);
#55186=AXIS2_PLACEMENT_3D('',#90620,#67809,#67810);
#55187=AXIS2_PLACEMENT_3D('',#90621,#67811,#67812);
#55188=AXIS2_PLACEMENT_3D('',#90623,#67813,#67814);
#55189=AXIS2_PLACEMENT_3D('',#90624,#67815,#67816);
#55190=AXIS2_PLACEMENT_3D('',#90626,#67817,#67818);
#55191=AXIS2_PLACEMENT_3D('',#90628,#67820,#67821);
#67792=DIRECTION('axis',(0.,0.,1.));
#67793=DIRECTION('refdir',(1.,0.,0.));
#67794=DIRECTION('center_axis',(1.,0.,0.));
#67795=DIRECTION('ref_axis',(0.,0.,-1.));
#67796=DIRECTION('center_axis',(-1.,0.,0.));
#67797=DIRECTION('ref_axis',(0.,-1.,1.83697019872103E-16));
#67798=DIRECTION('center_axis',(0.,-1.,-1.22464679914735E-16));
#67799=DIRECTION('ref_axis',(0.,-1.22464679914735E-16,1.));
#67800=DIRECTION('center_axis',(1.,0.,0.));
#67801=DIRECTION('ref_axis',(0.,-1.,3.06161699786838E-17));
#67802=DIRECTION('center_axis',(1.,0.,0.));
#67803=DIRECTION('ref_axis',(0.,-1.,3.06161699786838E-17));
#67804=DIRECTION('center_axis',(-1.,0.,0.));
#67805=DIRECTION('ref_axis',(0.,1.,0.));
#67806=DIRECTION('',(-0.707106781186548,-0.707106781186547,-8.65956056235493E-17));
#67807=DIRECTION('center_axis',(1.,0.,0.));
#67808=DIRECTION('ref_axis',(0.,0.,-1.));
#67809=DIRECTION('center_axis',(1.,0.,0.));
#67810=DIRECTION('ref_axis',(0.,0.,-1.));
#67811=DIRECTION('center_axis',(-1.,0.,0.));
#67812=DIRECTION('ref_axis',(0.,0.,1.));
#67813=DIRECTION('center_axis',(1.,0.,0.));
#67814=DIRECTION('ref_axis',(0.,0.,-1.));
#67815=DIRECTION('center_axis',(1.,0.,0.));
#67816=DIRECTION('ref_axis',(0.,1.,0.));
#67817=DIRECTION('center_axis',(1.,0.,0.));
#67818=DIRECTION('ref_axis',(0.,0.,-1.));
#67819=DIRECTION('',(-0.707106781186547,0.707106781186548,8.65956056235493E-17));
#67820=DIRECTION('center_axis',(1.,0.,0.));
#67821=DIRECTION('ref_axis',(0.,1.,0.));
#67822=DIRECTION('',(-1.,0.,0.));
#90607=CARTESIAN_POINT('',(0.,0.,0.));
#90608=CARTESIAN_POINT('Origin',(19.2,0.,0.));
#90609=CARTESIAN_POINT('',(20.,-2.53334006729474E-16,2.06862915010152));
#90610=CARTESIAN_POINT('Origin',(20.,0.,0.));
#90611=CARTESIAN_POINT('',(19.7656854249492,-3.22610491228314E-16,2.63431457505076));
#90612=CARTESIAN_POINT('Origin',(19.2,-2.53334006729474E-16,2.06862915010152));
#90613=CARTESIAN_POINT('',(19.7656854249492,-2.63431457505076,-3.22610491228314E-16));
#90614=CARTESIAN_POINT('Origin',(19.7656854249492,0.,-4.03263114035392E-16));
#90615=CARTESIAN_POINT('Origin',(19.7656854249492,0.,-4.03263114035392E-16));
#90616=CARTESIAN_POINT('Origin',(19.7,0.,0.));
#90617=CARTESIAN_POINT('',(19.4,-3.,-3.67394039744206E-16));
#90618=CARTESIAN_POINT('',(19.7,-2.7,-3.30654635769785E-16));
#90619=CARTESIAN_POINT('Origin',(19.4,0.,0.));
#90620=CARTESIAN_POINT('Origin',(20.,0.,0.));
#90621=CARTESIAN_POINT('Origin',(0.,2.4,0.));
#90622=CARTESIAN_POINT('',(-6.93889390390723E-17,-2.4,-2.93915231795365E-16));
#90623=CARTESIAN_POINT('Origin',(0.,0.,0.));
#90624=CARTESIAN_POINT('Origin',(0.3,0.,0.));
#90625=CARTESIAN_POINT('',(0.6,-3.,-3.67394039744206E-16));
#90626=CARTESIAN_POINT('Origin',(0.600000000000001,0.,0.));
#90627=CARTESIAN_POINT('',(0.3,-2.7,-3.30654635769785E-16));
#90628=CARTESIAN_POINT('Origin',(10.,0.,0.));
#90629=CARTESIAN_POINT('',(10.,-3.,-3.67394039744206E-16));
#94280=UNCERTAINTY_MEASURE_WITH_UNIT(LENGTH_MEASURE(0.01),#94302,
'DISTANCE_ACCURACY_VALUE',
'Maximum model space distance between geometric entities at asserted c
onnectivities');
#94285=UNCERTAINTY_MEASURE_WITH_UNIT(LENGTH_MEASURE(0.01),#94302,
'DISTANCE_ACCURACY_VALUE',
'Maximum model space distance between geometric entities at asserted c
onnectivities');
#94296=(
GEOMETRIC_REPRESENTATION_CONTEXT(3)
GLOBAL_UNCERTAINTY_ASSIGNED_CONTEXT((#94280))
GLOBAL_UNIT_ASSIGNED_CONTEXT((#94302,#94304,#94305))
REPRESENTATION_CONTEXT('','3D')
);
#94301=(
GEOMETRIC_REPRESENTATION_CONTEXT(3)
GLOBAL_UNCERTAINTY_ASSIGNED_CONTEXT((#94285))
GLOBAL_UNIT_ASSIGNED_CONTEXT((#94302,#94304,#94305))
REPRESENTATION_CONTEXT('','3D')
);
#94302=(
LENGTH_UNIT()
NAMED_UNIT(*)
SI_UNIT(.MILLI.,.METRE.)
);
#94304=(
NAMED_UNIT(*)
PLANE_ANGLE_UNIT()
SI_UNIT($,.RADIAN.)
);
#94305=(
NAMED_UNIT(*)
SI_UNIT($,.STERADIAN.)
SOLID_ANGLE_UNIT()
);
#94316=SHAPE_DEFINITION_REPRESENTATION(#94331,#94380);
#94331=PRODUCT_DEFINITION_SHAPE('',$,#94396);
#94380=SHAPE_REPRESENTATION('',(#55178),#94296);
#94385=PRODUCT_DEFINITION_CONTEXT('part definition',#94432,'design');
#94396=PRODUCT_DEFINITION('2026-10-11-08-26-44-599',
'10_ISO_8734_Dowel_6x20',#94411,#94385);
#94411=PRODUCT_DEFINITION_FORMATION('',$,#94444);
#94432=APPLICATION_CONTEXT(
'Core Data for Automotive Mechanical Design Process');
#94433=PRODUCT_CONTEXT('part definition',#94432,'mechanical');
#94444=PRODUCT('2026-10-11-08-26-44-599','10_ISO_8734_Dowel_6x20',$,(#94433));
#94589=COLOUR_RGB('Off White',0.89,0.88,0.83);
#94590=FILL_AREA_STYLE_COLOUR('',#94589);
#94591=FILL_AREA_STYLE('',(#94590));
#94592=SURFACE_STYLE_FILL_AREA(#94591);
#94593=SURFACE_SIDE_STYLE('',(#94592));
#94594=SURFACE_STYLE_USAGE(.BOTH.,#94593);
#94595=PRESENTATION_STYLE_ASSIGNMENT((#94594));
ENDSEC;
END-ISO-10303-21;
